ISO-10303-21;
HEADER;
/* Generated by software containing ST-Developer
 * from STEP Tools, Inc. (www.steptools.com) 
 */

FILE_DESCRIPTION(
/* description */ ('Manual rail carriage with stops'),
/* implementation_level */ '2;1');

FILE_NAME(
/* name */ 'Cap Screw - M6x25.step',
/* time_stamp */ '2026-10-27T18:54:27-07:00',
/* author */ (''),
/* organization */ (''),
/* preprocessor_version */ 'ST-DEVELOPER v20.2',
/* originating_system */ 'Autodesk Translation Framework v15.17.0.0',
/* authorisation */ '');

FILE_SCHEMA (('AUTOMOTIVE_DESIGN { 1 0 10303 214 3 1 1 }'));
ENDSEC;

DATA;
#10=MECHANICAL_DESIGN_GEOMETRIC_PRESENTATION_REPRESENTATION('',(#290),#8499);
#223=CONICAL_SURFACE('',#5593,0.475,0.785398163397449);
#224=CONICAL_SURFACE('',#5597,0.485,0.785398163397448);
#225=CONICAL_SURFACE('',#5601,0.31,0.463647609000806);
#226=CONICAL_SURFACE('',#5605,0.27,0.785398163397448);
#230=ORIENTED_CLOSED_SHELL('',*,#4962,.F.);
#234=BREP_WITH_VOIDS('Body1',#4961,(#230));
#254=SHAPE_REPRESENTATION_RELATIONSHIP('SRR','None',#8619,#272);
#272=ADVANCED_BREP_SHAPE_REPRESENTATION('',(#234),#8498);
#290=STYLED_ITEM('',(#8795),#234);
#379=FACE_BOUND('',#1169,.T.);
#566=PLANE('',#5591);
#567=PLANE('',#5599);
#568=PLANE('',#5607);
#569=PLANE('',#5608);
#570=PLANE('',#5609);
#571=PLANE('',#5610);
#572=PLANE('',#5611);
#573=PLANE('',#5612);
#574=PLANE('',#5613);
#575=PLANE('',#5614);
#576=PLANE('',#5615);
#825=FACE_OUTER_BOUND('',#1164,.T.);
#826=FACE_OUTER_BOUND('',#1165,.T.);
#827=FACE_OUTER_BOUND('',#1166,.T.);
#828=FACE_OUTER_BOUND('',#1167,.T.);
#829=FACE_OUTER_BOUND('',#1168,.T.);
#830=FACE_OUTER_BOUND('',#1170,.T.);
#831=FACE_OUTER_BOUND('',#1171,.T.);
#832=FACE_OUTER_BOUND('',#1172,.T.);
#833=FACE_OUTER_BOUND('',#1173,.T.);
#834=FACE_OUTER_BOUND('',#1174,.T.);
#835=FACE_OUTER_BOUND('',#1175,.T.);
#836=FACE_OUTER_BOUND('',#1176,.T.);
#837=FACE_OUTER_BOUND('',#1177,.T.);
#838=FACE_OUTER_BOUND('',#1178,.T.);
#839=FACE_OUTER_BOUND('',#1179,.T.);
#840=FACE_OUTER_BOUND('',#1180,.T.);
#841=FACE_OUTER_BOUND('',#1181,.T.);
#1164=EDGE_LOOP('',(#4560));
#1165=EDGE_LOOP('',(#4561,#4562,#4563,#4564));
#1166=EDGE_LOOP('',(#4565,#4566,#4567,#4568));
#1167=EDGE_LOOP('',(#4569,#4570,#4571,#4572));
#1168=EDGE_LOOP('',(#4573));
#1169=EDGE_LOOP('',(#4574));
#1170=EDGE_LOOP('',(#4575,#4576,#4577,#4578));
#1171=EDGE_LOOP('',(#4579,#4580,#4581,#4582));
#1172=EDGE_LOOP('',(#4583,#4584,#4585,#4586));
#1173=EDGE_LOOP('',(#4587));
#1174=EDGE_LOOP('',(#4588,#4589,#4590,#4591));
#1175=EDGE_LOOP('',(#4592,#4593,#4594,#4595));
#1176=EDGE_LOOP('',(#4596,#4597,#4598,#4599));
#1177=EDGE_LOOP('',(#4600,#4601,#4602,#4603));
#1178=EDGE_LOOP('',(#4604,#4605,#4606,#4607));
#1179=EDGE_LOOP('',(#4608,#4609,#4610,#4611));
#1180=EDGE_LOOP('',(#4612,#4613,#4614,#4615,#4616,#4617));
#1181=EDGE_LOOP('',(#4618,#4619,#4620,#4621,#4622,#4623));
#1658=LINE('',#8376,#2158);
#1659=LINE('',#8380,#2159);
#1660=LINE('',#8384,#2160);
#1661=LINE('',#8391,#2161);
#1662=LINE('',#8395,#2162);
#1663=LINE('',#8399,#2163);
#1664=LINE('',#8404,#2164);
#1665=LINE('',#8406,#2165);
#1666=LINE('',#8408,#2166);
#1667=LINE('',#8409,#2167);
#1668=LINE('',#8412,#2168);
#1669=LINE('',#8414,#2169);
#1670=LINE('',#8415,#2170);
#1671=LINE('',#8418,#2171);
#1672=LINE('',#8420,#2172);
#1673=LINE('',#8421,#2173);
#1674=LINE('',#8424,#2174);
#1675=LINE('',#8426,#2175);
#1676=LINE('',#8427,#2176);
#1677=LINE('',#8430,#2177);
#1678=LINE('',#8432,#2178);
#1679=LINE('',#8433,#2179);
#1680=LINE('',#8435,#2180);
#1681=LINE('',#8436,#2181);
#2158=VECTOR('',#6973,0.475);
#2159=VECTOR('',#6978,0.5);
#2160=VECTOR('',#6983,0.485);
#2161=VECTOR('',#6992,0.31);
#2162=VECTOR('',#6997,0.3);
#2163=VECTOR('',#7002,0.27);
#2164=VECTOR('',#7007,1.);
#2165=VECTOR('',#7008,1.);
#2166=VECTOR('',#7009,1.);
#2167=VECTOR('',#7010,1.);
#2168=VECTOR('',#7013,1.);
#2169=VECTOR('',#7014,1.);
#2170=VECTOR('',#7015,1.);
#2171=VECTOR('',#7018,1.);
#2172=VECTOR('',#7019,1.);
#2173=VECTOR('',#7020,1.);
#2174=VECTOR('',#7023,1.);
#2175=VECTOR('',#7024,1.);
#2176=VECTOR('',#7025,1.);
#2177=VECTOR('',#7028,1.);
#2178=VECTOR('',#7029,1.);
#2179=VECTOR('',#7030,1.);
#2180=VECTOR('',#7033,1.);
#2181=VECTOR('',#7034,1.);
#2304=CIRCLE('',#5592,0.45);
#2305=CIRCLE('',#5594,0.5);
#2306=CIRCLE('',#5596,0.5);
#2307=CIRCLE('',#5598,0.47);
#2308=CIRCLE('',#5600,0.32);
#2309=CIRCLE('',#5602,0.2942);
#2310=CIRCLE('',#5604,0.2942);
#2311=CIRCLE('',#5606,0.24);
#2708=VERTEX_POINT('',#8371);
#2709=VERTEX_POINT('',#8374);
#2710=VERTEX_POINT('',#8378);
#2711=VERTEX_POINT('',#8382);
#2712=VERTEX_POINT('',#8386);
#2713=VERTEX_POINT('',#8389);
#2714=VERTEX_POINT('',#8393);
#2715=VERTEX_POINT('',#8397);
#2716=VERTEX_POINT('',#8402);
#2717=VERTEX_POINT('',#8403);
#2718=VERTEX_POINT('',#8405);
#2719=VERTEX_POINT('',#8407);
#2720=VERTEX_POINT('',#8411);
#2721=VERTEX_POINT('',#8413);
#2722=VERTEX_POINT('',#8417);
#2723=VERTEX_POINT('',#8419);
#2724=VERTEX_POINT('',#8423);
#2725=VERTEX_POINT('',#8425);
#2726=VERTEX_POINT('',#8429);
#2727=VERTEX_POINT('',#8431);
#3328=EDGE_CURVE('',#2708,#2708,#2304,.T.);
#3329=EDGE_CURVE('',#2709,#2709,#2305,.T.);
#3330=EDGE_CURVE('',#2709,#2708,#1658,.T.);
#3331=EDGE_CURVE('',#2710,#2710,#2306,.T.);
#3332=EDGE_CURVE('',#2710,#2709,#1659,.T.);
#3333=EDGE_CURVE('',#2711,#2711,#2307,.T.);
#3334=EDGE_CURVE('',#2711,#2710,#1660,.T.);
#3335=EDGE_CURVE('',#2712,#2712,#2308,.T.);
#3336=EDGE_CURVE('',#2713,#2713,#2309,.F.);
#3337=EDGE_CURVE('',#2713,#2712,#1661,.T.);
#3338=EDGE_CURVE('',#2714,#2714,#2310,.F.);
#3339=EDGE_CURVE('',#2714,#2713,#1662,.T.);
#3340=EDGE_CURVE('',#2715,#2715,#2311,.T.);
#3341=EDGE_CURVE('',#2715,#2714,#1663,.T.);
#3342=EDGE_CURVE('',#2716,#2717,#1664,.T.);
#3343=EDGE_CURVE('',#2717,#2718,#1665,.T.);
#3344=EDGE_CURVE('',#2718,#2719,#1666,.T.);
#3345=EDGE_CURVE('',#2716,#2719,#1667,.T.);
#3346=EDGE_CURVE('',#2717,#2720,#1668,.T.);
#3347=EDGE_CURVE('',#2720,#2721,#1669,.T.);
#3348=EDGE_CURVE('',#2721,#2718,#1670,.T.);
#3349=EDGE_CURVE('',#2720,#2722,#1671,.T.);
#3350=EDGE_CURVE('',#2722,#2723,#1672,.T.);
#3351=EDGE_CURVE('',#2723,#2721,#1673,.T.);
#3352=EDGE_CURVE('',#2722,#2724,#1674,.T.);
#3353=EDGE_CURVE('',#2724,#2725,#1675,.T.);
#3354=EDGE_CURVE('',#2725,#2723,#1676,.T.);
#3355=EDGE_CURVE('',#2724,#2726,#1677,.T.);
#3356=EDGE_CURVE('',#2726,#2727,#1678,.T.);
#3357=EDGE_CURVE('',#2727,#2725,#1679,.T.);
#3358=EDGE_CURVE('',#2726,#2716,#1680,.T.);
#3359=EDGE_CURVE('',#2719,#2727,#1681,.T.);
#4560=ORIENTED_EDGE('',*,*,#3328,.F.);
#4561=ORIENTED_EDGE('',*,*,#3329,.F.);
#4562=ORIENTED_EDGE('',*,*,#3330,.T.);
#4563=ORIENTED_EDGE('',*,*,#3328,.T.);
#4564=ORIENTED_EDGE('',*,*,#3330,.F.);
#4565=ORIENTED_EDGE('',*,*,#3331,.F.);
#4566=ORIENTED_EDGE('',*,*,#3332,.T.);
#4567=ORIENTED_EDGE('',*,*,#3329,.T.);
#4568=ORIENTED_EDGE('',*,*,#3332,.F.);
#4569=ORIENTED_EDGE('',*,*,#3333,.F.);
#4570=ORIENTED_EDGE('',*,*,#3334,.T.);
#4571=ORIENTED_EDGE('',*,*,#3331,.T.);
#4572=ORIENTED_EDGE('',*,*,#3334,.F.);
#4573=ORIENTED_EDGE('',*,*,#3333,.T.);
#4574=ORIENTED_EDGE('',*,*,#3335,.F.);
#4575=ORIENTED_EDGE('',*,*,#3336,.F.);
#4576=ORIENTED_EDGE('',*,*,#3337,.T.);
#4577=ORIENTED_EDGE('',*,*,#3335,.T.);
#4578=ORIENTED_EDGE('',*,*,#3337,.F.);
#4579=ORIENTED_EDGE('',*,*,#3338,.F.);
#4580=ORIENTED_EDGE('',*,*,#3339,.T.);
#4581=ORIENTED_EDGE('',*,*,#3336,.T.);
#4582=ORIENTED_EDGE('',*,*,#3339,.F.);
#4583=ORIENTED_EDGE('',*,*,#3340,.F.);
#4584=ORIENTED_EDGE('',*,*,#3341,.T.);
#4585=ORIENTED_EDGE('',*,*,#3338,.T.);
#4586=ORIENTED_EDGE('',*,*,#3341,.F.);
#4587=ORIENTED_EDGE('',*,*,#3340,.T.);
#4588=ORIENTED_EDGE('',*,*,#3342,.T.);
#4589=ORIENTED_EDGE('',*,*,#3343,.T.);
#4590=ORIENTED_EDGE('',*,*,#3344,.T.);
#4591=ORIENTED_EDGE('',*,*,#3345,.F.);
#4592=ORIENTED_EDGE('',*,*,#3346,.T.);
#4593=ORIENTED_EDGE('',*,*,#3347,.T.);
#4594=ORIENTED_EDGE('',*,*,#3348,.T.);
#4595=ORIENTED_EDGE('',*,*,#3343,.F.);
#4596=ORIENTED_EDGE('',*,*,#3349,.T.);
#4597=ORIENTED_EDGE('',*,*,#3350,.T.);
#4598=ORIENTED_EDGE('',*,*,#3351,.T.);
#4599=ORIENTED_EDGE('',*,*,#3347,.F.);
#4600=ORIENTED_EDGE('',*,*,#3352,.T.);
#4601=ORIENTED_EDGE('',*,*,#3353,.T.);
#4602=ORIENTED_EDGE('',*,*,#3354,.T.);
#4603=ORIENTED_EDGE('',*,*,#3350,.F.);
#4604=ORIENTED_EDGE('',*,*,#3355,.T.);
#4605=ORIENTED_EDGE('',*,*,#3356,.T.);
#4606=ORIENTED_EDGE('',*,*,#3357,.T.);
#4607=ORIENTED_EDGE('',*,*,#3353,.F.);
#4608=ORIENTED_EDGE('',*,*,#3358,.T.);
#4609=ORIENTED_EDGE('',*,*,#3345,.T.);
#4610=ORIENTED_EDGE('',*,*,#3359,.T.);
#4611=ORIENTED_EDGE('',*,*,#3356,.F.);
#4612=ORIENTED_EDGE('',*,*,#3358,.F.);
#4613=ORIENTED_EDGE('',*,*,#3355,.F.);
#4614=ORIENTED_EDGE('',*,*,#3352,.F.);
#4615=ORIENTED_EDGE('',*,*,#3349,.F.);
#4616=ORIENTED_EDGE('',*,*,#3346,.F.);
#4617=ORIENTED_EDGE('',*,*,#3342,.F.);
#4618=ORIENTED_EDGE('',*,*,#3359,.F.);
#4619=ORIENTED_EDGE('',*,*,#3344,.F.);
#4620=ORIENTED_EDGE('',*,*,#3348,.F.);
#4621=ORIENTED_EDGE('',*,*,#3351,.F.);
#4622=ORIENTED_EDGE('',*,*,#3354,.F.);
#4623=ORIENTED_EDGE('',*,*,#3357,.F.);
#4674=CYLINDRICAL_SURFACE('',#5595,0.5);
#4675=CYLINDRICAL_SURFACE('',#5603,0.2942);
#4924=ADVANCED_FACE('',(#825),#566,.T.);
#4925=ADVANCED_FACE('',(#826),#223,.T.);
#4926=ADVANCED_FACE('',(#827),#4674,.T.);
#4927=ADVANCED_FACE('',(#828),#224,.T.);
#4928=ADVANCED_FACE('',(#829,#379),#567,.T.);
#4929=ADVANCED_FACE('',(#830),#225,.T.);
#4930=ADVANCED_FACE('',(#831),#4675,.T.);
#4931=ADVANCED_FACE('',(#832),#226,.T.);
#4932=ADVANCED_FACE('',(#833),#568,.T.);
#4933=ADVANCED_FACE('',(#834),#569,.F.);
#4934=ADVANCED_FACE('',(#835),#570,.F.);
#4935=ADVANCED_FACE('',(#836),#571,.F.);
#4936=ADVANCED_FACE('',(#837),#572,.F.);
#4937=ADVANCED_FACE('',(#838),#573,.F.);
#4938=ADVANCED_FACE('',(#839),#574,.F.);
#4939=ADVANCED_FACE('',(#840),#575,.F.);
#4940=ADVANCED_FACE('',(#841),#576,.F.);
#4961=CLOSED_SHELL('',(#4924,#4925,#4926,#4927,#4928,#4929,#4930,#4931,
#4932));
#4962=CLOSED_SHELL('',(#4933,#4934,#4935,#4936,#4937,#4938,#4939,#4940));
#5590=AXIS2_PLACEMENT_3D('',#8369,#6963,#6964);
#5591=AXIS2_PLACEMENT_3D('',#8370,#6965,#6966);
#5592=AXIS2_PLACEMENT_3D('',#8372,#6967,#6968);
#5593=AXIS2_PLACEMENT_3D('',#8373,#6969,#6970);
#5594=AXIS2_PLACEMENT_3D('',#8375,#6971,#6972);
#5595=AXIS2_PLACEMENT_3D('',#8377,#6974,#6975);
#5596=AXIS2_PLACEMENT_3D('',#8379,#6976,#6977);
#5597=AXIS2_PLACEMENT_3D('',#8381,#6979,#6980);
#5598=AXIS2_PLACEMENT_3D('',#8383,#6981,#6982);
#5599=AXIS2_PLACEMENT_3D('',#8385,#6984,#6985);
#5600=AXIS2_PLACEMENT_3D('',#8387,#6986,#6987);
#5601=AXIS2_PLACEMENT_3D('',#8388,#6988,#6989);
#5602=AXIS2_PLACEMENT_3D('',#8390,#6990,#6991);
#5603=AXIS2_PLACEMENT_3D('',#8392,#6993,#6994);
#5604=AXIS2_PLACEMENT_3D('',#8394,#6995,#6996);
#5605=AXIS2_PLACEMENT_3D('',#8396,#6998,#6999);
#5606=AXIS2_PLACEMENT_3D('',#8398,#7000,#7001);
#5607=AXIS2_PLACEMENT_3D('',#8400,#7003,#7004);
#5608=AXIS2_PLACEMENT_3D('',#8401,#7005,#7006);
#5609=AXIS2_PLACEMENT_3D('',#8410,#7011,#7012);
#5610=AXIS2_PLACEMENT_3D('',#8416,#7016,#7017);
#5611=AXIS2_PLACEMENT_3D('',#8422,#7021,#7022);
#5612=AXIS2_PLACEMENT_3D('',#8428,#7026,#7027);
#5613=AXIS2_PLACEMENT_3D('',#8434,#7031,#7032);
#5614=AXIS2_PLACEMENT_3D('',#8437,#7035,#7036);
#5615=AXIS2_PLACEMENT_3D('',#8438,#7037,#7038);
#6963=DIRECTION('axis',(0.,0.,1.));
#6964=DIRECTION('refdir',(1.,0.,0.));
#6965=DIRECTION('center_axis',(0.,1.,0.));
#6966=DIRECTION('ref_axis',(0.,0.,1.));
#6967=DIRECTION('center_axis',(0.,-1.,0.));
#6968=DIRECTION('ref_axis',(1.,0.,0.));
#6969=DIRECTION('center_axis',(0.,-1.,0.));
#6970=DIRECTION('ref_axis',(1.,0.,0.));
#6971=DIRECTION('center_axis',(0.,-1.,0.));
#6972=DIRECTION('ref_axis',(1.,0.,0.));
#6973=DIRECTION('',(0.707106781186548,0.707106781186547,8.65956056235494E-17));
#6974=DIRECTION('center_axis',(0.,-1.,0.));
#6975=DIRECTION('ref_axis',(1.,0.,0.));
#6976=DIRECTION('center_axis',(0.,-1.,0.));
#6977=DIRECTION('ref_axis',(1.,0.,0.));
#6978=DIRECTION('',(0.,1.,0.));
#6979=DIRECTION('center_axis',(0.,1.,0.));
#6980=DIRECTION('ref_axis',(1.,0.,0.));
#6981=DIRECTION('center_axis',(0.,-1.,0.));
#6982=DIRECTION('ref_axis',(1.,0.,0.));
#6983=DIRECTION('',(-0.707106781186547,0.707106781186548,-8.65956056235493E-17));
#6984=DIRECTION('center_axis',(0.,-1.,0.));
#6985=DIRECTION('ref_axis',(0.,0.,-1.));
#6986=DIRECTION('center_axis',(0.,-1.,0.));
#6987=DIRECTION('ref_axis',(1.,0.,0.));
#6988=DIRECTION('center_axis',(0.,1.,0.));
#6989=DIRECTION('ref_axis',(1.,0.,0.));
#6990=DIRECTION('center_axis',(0.,1.,0.));
#6991=DIRECTION('ref_axis',(1.,0.,0.));
#6992=DIRECTION('',(-0.447213595499958,0.894427190999916,-5.47678698264203E-17));
#6993=DIRECTION('center_axis',(0.,-1.,0.));
#6994=DIRECTION('ref_axis',(1.,0.,0.));
#6995=DIRECTION('center_axis',(0.,1.,0.));
#6996=DIRECTION('ref_axis',(1.,0.,0.));
#6997=DIRECTION('',(0.,1.,0.));
#6998=DIRECTION('center_axis',(0.,1.,0.));
#6999=DIRECTION('ref_axis',(1.,0.,0.));
#7000=DIRECTION('center_axis',(0.,-1.,0.));
#7001=DIRECTION('ref_axis',(1.,0.,0.));
#7002=DIRECTION('',(-0.707106781186547,0.707106781186548,-8.65956056235493E-17));
#7003=DIRECTION('center_axis',(0.,-1.,0.));
#7004=DIRECTION('ref_axis',(0.,0.,-1.));
#7005=DIRECTION('center_axis',(0.866025403784439,0.,-0.5));
#7006=DIRECTION('ref_axis',(0.5,0.,0.866025403784439));
#7007=DIRECTION('',(-0.5,0.,-0.866025403784439));
#7008=DIRECTION('',(0.,-1.,0.));
#7009=DIRECTION('',(0.5,0.,0.866025403784439));
#7010=DIRECTION('',(0.,-1.,0.));
#7011=DIRECTION('center_axis',(1.92296268638356E-16,0.,-1.));
#7012=DIRECTION('ref_axis',(1.,0.,1.92296268638356E-16));
#7013=DIRECTION('',(-1.,0.,-1.92296268638356E-16));
#7014=DIRECTION('',(0.,-1.,0.));
#7015=DIRECTION('',(1.,0.,1.92296268638356E-16));
#7016=DIRECTION('center_axis',(-0.866025403784439,0.,-0.5));
#7017=DIRECTION('ref_axis',(0.5,0.,-0.866025403784439));
#7018=DIRECTION('',(-0.5,0.,0.866025403784438));
#7019=DIRECTION('',(0.,-1.,0.));
#7020=DIRECTION('',(0.5,0.,-0.866025403784438));
#7021=DIRECTION('center_axis',(-0.866025403784439,0.,0.5));
#7022=DIRECTION('ref_axis',(-0.5,0.,-0.866025403784439));
#7023=DIRECTION('',(0.5,0.,0.866025403784439));
#7024=DIRECTION('',(0.,-1.,0.));
#7025=DIRECTION('',(-0.5,0.,-0.866025403784439));
#7026=DIRECTION('center_axis',(-1.92296268638356E-16,0.,1.));
#7027=DIRECTION('ref_axis',(-1.,0.,-1.92296268638356E-16));
#7028=DIRECTION('',(1.,0.,1.92296268638356E-16));
#7029=DIRECTION('',(0.,-1.,0.));
#7030=DIRECTION('',(-1.,0.,-1.92296268638356E-16));
#7031=DIRECTION('center_axis',(0.866025403784439,0.,0.5));
#7032=DIRECTION('ref_axis',(-0.5,0.,0.866025403784439));
#7033=DIRECTION('',(0.5,0.,-0.866025403784439));
#7034=DIRECTION('',(-0.5,0.,0.866025403784439));
#7035=DIRECTION('center_axis',(0.,1.,0.));
#7036=DIRECTION('ref_axis',(1.,0.,0.));
#7037=DIRECTION('center_axis',(0.,-1.,0.));
#7038=DIRECTION('ref_axis',(0.,0.,-1.));
#8369=CARTESIAN_POINT('',(0.,0.,0.));
#8370=CARTESIAN_POINT('Origin',(0.45,0.6,0.));
#8371=CARTESIAN_POINT('',(-0.45,0.6,-5.51091059616309E-17));
#8372=CARTESIAN_POINT('Origin',(0.,0.6,0.));
#8373=CARTESIAN_POINT('Origin',(0.,0.575,0.));
#8374=CARTESIAN_POINT('',(-0.5,0.55,-6.12323399573677E-17));
#8375=CARTESIAN_POINT('Origin',(0.,0.55,0.));
#8376=CARTESIAN_POINT('',(-0.475,0.575,-5.81707229594993E-17));
#8377=CARTESIAN_POINT('Origin',(0.,0.29,0.));
#8378=CARTESIAN_POINT('',(-0.5,0.0299999999999998,-6.12323399573677E-17));
#8379=CARTESIAN_POINT('Origin',(0.,0.0299999999999998,0.));
#8380=CARTESIAN_POINT('',(-0.5,0.29,-6.12323399573677E-17));
#8381=CARTESIAN_POINT('Origin',(0.,0.0150000000000001,0.));
#8382=CARTESIAN_POINT('',(-0.47,7.11236625150491E-17,-5.75583995599256E-17));
#8383=CARTESIAN_POINT('Origin',(0.,0.,0.));
#8384=CARTESIAN_POINT('',(-0.485,0.0150000000000001,-5.93953697586466E-17));
#8385=CARTESIAN_POINT('Origin',(0.32,0.,0.));
#8386=CARTESIAN_POINT('',(-0.32,-6.93889390390723E-18,-3.91886975727153E-17));
#8387=CARTESIAN_POINT('Origin',(0.,0.,0.));
#8388=CARTESIAN_POINT('Origin',(0.,-0.02,0.));
#8389=CARTESIAN_POINT('',(-0.2942,-0.0515999999999999,3.60291088309151E-17));
#8390=CARTESIAN_POINT('Origin',(0.,-0.0515999999999999,0.));
#8391=CARTESIAN_POINT('',(-0.31,-0.02,-3.7964050773568E-17));
#8392=CARTESIAN_POINT('Origin',(0.,-1.24,0.));
#8393=CARTESIAN_POINT('',(-0.2942,-2.4458,3.60291088309151E-17));
#8394=CARTESIAN_POINT('Origin',(0.,-2.4458,0.));
#8395=CARTESIAN_POINT('',(-0.2942,-1.24,-3.60291088309151E-17));
#8396=CARTESIAN_POINT('Origin',(0.,-2.47,0.));
#8397=CARTESIAN_POINT('',(-0.24,-2.5,-2.93915231795365E-17));
#8398=CARTESIAN_POINT('Origin',(0.,-2.5,0.));
#8399=CARTESIAN_POINT('',(-0.27,-2.47,-3.30654635769785E-17));
#8400=CARTESIAN_POINT('Origin',(0.,-2.5,0.));
#8401=CARTESIAN_POINT('Origin',(0.144337567297406,-0.6,-0.25));
#8402=CARTESIAN_POINT('',(0.288675134594813,-0.6,0.));
#8403=CARTESIAN_POINT('',(0.144337567297406,-0.6,-0.25));
#8404=CARTESIAN_POINT('',(0.288675134594813,-0.6,0.));
#8405=CARTESIAN_POINT('',(0.144337567297406,-0.96,-0.25));
#8406=CARTESIAN_POINT('',(0.144337567297406,-0.6,-0.25));
#8407=CARTESIAN_POINT('',(0.288675134594813,-0.96,0.));
#8408=CARTESIAN_POINT('',(0.288675134594813,-0.96,0.));
#8409=CARTESIAN_POINT('',(0.288675134594813,-0.6,0.));
#8410=CARTESIAN_POINT('Origin',(-0.144337567297406,-0.6,-0.25));
#8411=CARTESIAN_POINT('',(-0.144337567297406,-0.6,-0.25));
#8412=CARTESIAN_POINT('',(0.144337567297406,-0.6,-0.25));
#8413=CARTESIAN_POINT('',(-0.144337567297406,-0.96,-0.25));
#8414=CARTESIAN_POINT('',(-0.144337567297406,-0.6,-0.25));
#8415=CARTESIAN_POINT('',(0.144337567297406,-0.96,-0.25));
#8416=CARTESIAN_POINT('Origin',(-0.288675134594813,-0.6,-8.32667268468867E-17));
#8417=CARTESIAN_POINT('',(-0.288675134594813,-0.6,-3.53525079574969E-17));
#8418=CARTESIAN_POINT('',(-0.144337567297406,-0.6,-0.25));
#8419=CARTESIAN_POINT('',(-0.288675134594813,-0.96,-5.55111512312578E-17));
#8420=CARTESIAN_POINT('',(-0.288675134594813,-0.6,-3.53525079574969E-17));
#8421=CARTESIAN_POINT('',(-0.144337567297406,-0.96,-0.25));
#8422=CARTESIAN_POINT('Origin',(-0.144337567297407,-0.6,0.25));
#8423=CARTESIAN_POINT('',(-0.144337567297407,-0.6,0.25));
#8424=CARTESIAN_POINT('',(-0.288675134594813,-0.6,-3.53525079574969E-17));
#8425=CARTESIAN_POINT('',(-0.144337567297407,-0.96,0.25));
#8426=CARTESIAN_POINT('',(-0.144337567297407,-0.6,0.25));
#8427=CARTESIAN_POINT('',(-0.288675134594813,-0.96,-3.53525079574969E-17));
#8428=CARTESIAN_POINT('Origin',(0.144337567297406,-0.6,0.25));
#8429=CARTESIAN_POINT('',(0.144337567297406,-0.6,0.25));
#8430=CARTESIAN_POINT('',(-0.144337567297407,-0.6,0.25));
#8431=CARTESIAN_POINT('',(0.144337567297406,-0.96,0.25));
#8432=CARTESIAN_POINT('',(0.144337567297406,-0.6,0.25));
#8433=CARTESIAN_POINT('',(-0.144337567297407,-0.96,0.25));
#8434=CARTESIAN_POINT('Origin',(0.288675134594813,-0.6,0.));
#8435=CARTESIAN_POINT('',(0.144337567297406,-0.6,0.25));
#8436=CARTESIAN_POINT('',(0.144337567297406,-0.96,0.25));
#8437=CARTESIAN_POINT('Origin',(0.,-0.6,0.));
#8438=CARTESIAN_POINT('Origin',(0.,-0.96,0.));
#8475=UNCERTAINTY_MEASURE_WITH_UNIT(LENGTH_MEASURE(0.001),#8500,
'DISTANCE_ACCURACY_VALUE',
'Maximum model space distance between geometric entities at asserted c
onnectivities');
#8476=UNCERTAINTY_MEASURE_WITH_UNIT(LENGTH_MEASURE(0.001),#8500,
'DISTANCE_ACCURACY_VALUE',
'Maximum model space distance between geometric entities at asserted c
onnectivities');
#8498=(
GEOMETRIC_REPRESENTATION_CONTEXT(3)
GLOBAL_UNCERTAINTY_ASSIGNED_CONTEXT((#8475))
GLOBAL_UNIT_ASSIGNED_CONTEXT((#8500,#8502,#8503))
REPRESENTATION_CONTEXT('','3D')
);
#8499=(
GEOMETRIC_REPRESENTATION_CONTEXT(3)
GLOBAL_UNCERTAINTY_ASSIGNED_CONTEXT((#8476))
GLOBAL_UNIT_ASSIGNED_CONTEXT((#8500,#8502,#8503))
REPRESENTATION_CONTEXT('','3D')
);
#8500=(
LENGTH_UNIT()
NAMED_UNIT(*)
SI_UNIT(.CENTI.,.METRE.)
);
#8502=(
NAMED_UNIT(*)
PLANE_ANGLE_UNIT()
SI_UNIT($,.RADIAN.)
);
#8503=(
NAMED_UNIT(*)
SI_UNIT($,.STERADIAN.)
SOLID_ANGLE_UNIT()
);
#8525=SHAPE_DEFINITION_REPRESENTATION(#8582,#8619);
#8582=PRODUCT_DEFINITION_SHAPE('',$,#8642);
#8619=SHAPE_REPRESENTATION('',(#5590),#8498);
#8620=PRODUCT_DEFINITION_CONTEXT('part definition',#8688,'design');
#8642=PRODUCT_DEFINITION('Cap Screw - M6x25','Cap Screw - M6x25',#8664,
#8620);
#8664=PRODUCT_DEFINITION_FORMATION('',$,#8711);
#8688=APPLICATION_CONTEXT(
'Core Data for Automotive Mechanical Design Process');
#8689=PRODUCT_CONTEXT('part definition',#8688,'mechanical');
#8711=PRODUCT('Cap Screw - M6x25','Cap Screw - M6x25',
'Cap Screw - M6x25',(#8689));
#8789=COLOUR_RGB('Black',0.12,0.14,0.17);
#8790=FILL_AREA_STYLE_COLOUR('',#8789);
#8791=FILL_AREA_STYLE('',(#8790));
#8792=SURFACE_STYLE_FILL_AREA(#8791);
#8793=SURFACE_SIDE_STYLE('',(#8792));
#8794=SURFACE_STYLE_USAGE(.BOTH.,#8793);
#8795=PRESENTATION_STYLE_ASSIGNMENT((#8794));
ENDSEC;
END-ISO-10303-21;
